ISO-10303-21;
HEADER;
FILE_DESCRIPTION (('STEP AP214'),
    '1' );
FILE_NAME ('CIRCLIP DIN 471 - 25 × 1.2_GB_CONNECTING_PIECE_RING_RRA 25.step',
    '2026-09-30T12:41:04',
    ( '' ),
    ( '' ),
    'SwSTEP 2.0',
    'SolidWorks 2026',
    '' );
FILE_SCHEMA (( 'AUTOMOTIVE_DESIGN' ));
ENDSEC;

DATA;
#100=DIRECTION ( 'NONE',  ( 0.000000000000000000, 0.000000000000000000, 1.000000000000000000 ) ) ;
#199=VERTEX_POINT ( 'NONE', #18124 ) ;
#274=CYLINDRICAL_SURFACE ( 'NONE', #40603, 1.000000000000000888 ) ;
#284=CARTESIAN_POINT ( 'NONE',  ( 8.452893869119503023, -12.51233732111638375, -1.199999999999999956 ) ) ;
#289=CARTESIAN_POINT ( 'NONE',  ( 4.250000000000000000, -13.95926121303099343, 0.000000000000000000 ) ) ;
#350=LINE ( 'NONE', #7467, #9858 ) ;
#403=FILL_AREA_STYLE ('',( #33451 ) ) ;
#441=VERTEX_POINT ( 'NONE', #27431 ) ;
#453=EDGE_CURVE ( 'NONE', #25264, #47247, #1479, .T. ) ;
#658=LINE ( 'NONE', #45694, #5225 ) ;
#680=FACE_OUTER_BOUND ( 'NONE', #41723, .T. ) ;
#695=APPLICATION_CONTEXT ( 'automotive_design' ) ;
#892=ORIENTED_EDGE ( 'NONE', *, *, #13818, .F. ) ;
#941=DIRECTION ( 'NONE',  ( 0.1736481776669309418, -0.9848077530122080203, 0.000000000000000000 ) ) ;
#1045=ORIENTED_EDGE ( 'NONE', *, *, #3920, .T. ) ;
#1143=( NAMED_UNIT ( * ) PLANE_ANGLE_UNIT ( ) SI_UNIT ( $, .RADIAN. ) );
#1161=ORIENTED_EDGE ( 'NONE', *, *, #38046, .F. ) ;
#1286=VERTEX_POINT ( 'NONE', #12623 ) ;
#1343=AXIS2_PLACEMENT_3D ( 'NONE', #35872, #24626, #2337 ) ;
#1351=DIRECTION ( 'NONE',  ( -0.000000000000000000, -0.000000000000000000, -1.000000000000000000 ) ) ;
#1372=CARTESIAN_POINT ( 'NONE',  ( 0.000000000000000000, 0.000000000000000000, 0.000000000000000000 ) ) ;
#1458=CARTESIAN_POINT ( 'NONE',  ( 4.250000000000000000, -13.95926121303099343, -1.199999999999999956 ) ) ;
#1479=LINE ( 'NONE', #43078, #28583 ) ;
#1547=ORIENTED_EDGE ( 'NONE', *, *, #8949, .T. ) ;
#1589=DIRECTION ( 'NONE',  ( -0.000000000000000000, 0.000000000000000000, -1.000000000000000000 ) ) ;
#1802=DIRECTION ( 'NONE',  ( 0.000000000000000000, 0.000000000000000000, 1.000000000000000000 ) ) ;
#1823=ADVANCED_FACE ( 'NONE', ( #24238 ), #47696, .F. ) ;
#1883=PRODUCT ( 'CIRCLIP DIN 471 - 25 \X2\00d7\X0\ 1.2_GB_CONNECTING_PIECE_RING_RRA 25', 'CIRCLIP DIN 471 - 25 \X2\00d7\X0\ 1.2_GB_CONNECTING_PIECE_RING_RRA 25', '', ( #9214 ) ) ;
#1903=ORIENTED_EDGE ( 'NONE', *, *, #27770, .T. ) ;
#1952=ORIENTED_EDGE ( 'NONE', *, *, #6865, .F. ) ;
#2012=AXIS2_PLACEMENT_3D ( 'NONE', #16866, #5362, #42317 ) ;
#2337=DIRECTION ( 'NONE',  ( 1.000000000000000000, 0.000000000000000000, 0.000000000000000000 ) ) ;
#2426=DIRECTION ( 'NONE',  ( 0.000000000000000000, 0.000000000000000000, 1.000000000000000000 ) ) ;
#2455=DIRECTION ( 'NONE',  ( 1.000000000000000000, 0.000000000000000000, 0.000000000000000000 ) ) ;
#2586=ADVANCED_FACE ( 'NONE', ( #14317 ), #33161, .F. ) ;
#2648=AXIS2_PLACEMENT_3D ( 'NONE', #16804, #29731, #3056 ) ;
#2772=EDGE_LOOP ( 'NONE', ( #27994, #34696 ) ) ;
#2800=DIRECTION ( 'NONE',  ( 1.000000000000000000, 0.000000000000000000, 0.000000000000000000 ) ) ;
#2902=DIRECTION ( 'NONE',  ( 1.000000000000000000, 0.000000000000000000, 0.000000000000000000 ) ) ;
#2932=EDGE_CURVE ( 'NONE', #28331, #22374, #13740, .T. ) ;
#2950=ORIENTED_EDGE ( 'NONE', *, *, #45645, .F. ) ;
#2997=STYLED_ITEM ( 'NONE', ( #8975 ), #27490 ) ;
#3052=CIRCLE ( 'NONE', #17104, 1.000000000000000888 ) ;
#3056=DIRECTION ( 'NONE',  ( 1.000000000000000000, 0.000000000000000000, 0.000000000000000000 ) ) ;
#3127=EDGE_CURVE ( 'NONE', #199, #24143, #42575, .T. ) ;
#3173=PRODUCT_DEFINITION_CONTEXT ( 'detailed design', #695, 'design' ) ;
#3207=DIRECTION ( 'NONE',  ( 0.000000000000000000, 0.000000000000000000, 1.000000000000000000 ) ) ;
#3394=DIRECTION ( 'NONE',  ( 9.814797785686868941E-17, -1.000000000000000000, 0.000000000000000000 ) ) ;
#3399=FACE_OUTER_BOUND ( 'NONE', #29085, .T. ) ;
#3414=ORIENTED_EDGE ( 'NONE', *, *, #35958, .T. ) ;
#3474=DIRECTION ( 'NONE',  ( -1.000000000000000000, 0.000000000000000000, 0.000000000000000000 ) ) ;
#3667=DIRECTION ( 'NONE',  ( 1.000000000000000000, 0.000000000000000000, 0.000000000000000000 ) ) ;
#3707=ORIENTED_EDGE ( 'NONE', *, *, #21900, .F. ) ;
#3919=ADVANCED_FACE ( 'NONE', ( #19422, #29973, #45154 ), #33879, .F. ) ;
#3920=EDGE_CURVE ( 'NONE', #1286, #11028, #350, .T. ) ;
#3972=DIRECTION ( 'NONE',  ( 0.000000000000000000, 0.000000000000000000, 1.000000000000000000 ) ) ;
#4018=DIRECTION ( 'NONE',  ( 0.000000000000000000, 0.000000000000000000, -1.000000000000000000 ) ) ;
#4156=ORIENTED_EDGE ( 'NONE', *, *, #44088, .F. ) ;
#4183=VECTOR ( 'NONE', #21852, 1000.000000000000000 ) ;
#4337=AXIS2_PLACEMENT_3D ( 'NONE', #9639, #1589, #20183 ) ;
#4475=AXIS2_PLACEMENT_3D ( 'NONE', #9263, #31559, #35924 ) ;
#4532=VERTEX_POINT ( 'NONE', #27434 ) ;
#4547=CARTESIAN_POINT ( 'NONE',  ( 7.468086116107294004, -12.33868914344945189, 0.000000000000000000 ) ) ;
#4611=ORIENTED_EDGE ( 'NONE', *, *, #14144, .F. ) ;
#4630=EDGE_CURVE ( 'NONE', #5367, #29152, #14975, .T. ) ;
#4839=DIRECTION ( 'NONE',  ( 1.000000000000000000, 0.000000000000000000, 0.000000000000000000 ) ) ;
#4843=ORIENTED_EDGE ( 'NONE', *, *, #30448, .F. ) ;
#4929=DIRECTION ( 'NONE',  ( 1.000000000000000000, 0.000000000000000000, 0.000000000000000000 ) ) ;
#4977=CARTESIAN_POINT ( 'NONE',  ( 7.893099573151324044, -11.68370571044642503, 0.000000000000000000 ) ) ;
#4982=EDGE_CURVE ( 'NONE', #17248, #25278, #37537, .T. ) ;
#5225=VECTOR ( 'NONE', #12181, 1000.000000000000000 ) ;
#5313=FILL_AREA_STYLE_COLOUR ( '', #21751 ) ;
#5316=ORIENTED_EDGE ( 'NONE', *, *, #17076, .T. ) ;
#5362=DIRECTION ( 'NONE',  ( 0.000000000000000000, 0.000000000000000000, 1.000000000000000000 ) ) ;
#5367=VERTEX_POINT ( 'NONE', #4977 ) ;
#5398=ORIENTED_EDGE ( 'NONE', *, *, #44088, .T. ) ;
#5506=DIRECTION ( 'NONE',  ( -1.000000000000000000, 0.000000000000000000, 0.000000000000000000 ) ) ;
#5672=CIRCLE ( 'NONE', #11153, 14.09999999999999964 ) ;
#5744=FACE_BOUND ( 'NONE', #42512, .T. ) ;
#5750=VECTOR ( 'NONE', #23643, 1000.000000000000000 ) ;
#5776=ORIENTED_EDGE ( 'NONE', *, *, #12444, .T. ) ;
#5972=CARTESIAN_POINT ( 'NONE',  ( 0.000000000000000000, 0.000000000000000000, -1.199999999999999956 ) ) ;
#6021=DIRECTION ( 'NONE',  ( -1.000000000000000000, 0.000000000000000000, 0.000000000000000000 ) ) ;
#6035=ORIENTED_EDGE ( 'NONE', *, *, #36120, .F. ) ;
#6051=VERTEX_POINT ( 'NONE', #18811 ) ;
#6075=ADVANCED_FACE ( 'NONE', ( #3399 ), #44293, .T. ) ;
#6174=CIRCLE ( 'NONE', #43694, 16.00000000000000000 ) ;
#6291=VERTEX_POINT ( 'NONE', #13662 ) ;
#6297=DIRECTION ( 'NONE',  ( 0.9848077530122080203, -0.1736481776669309696, 0.000000000000000000 ) ) ;
#6311=EDGE_CURVE ( 'NONE', #11482, #7668, #46951, .T. ) ;
#6603=CARTESIAN_POINT ( 'NONE',  ( -8.452893869119503023, -12.51233732111638375, -1.199999999999999956 ) ) ;
#6619=DIRECTION ( 'NONE',  ( 0.000000000000000000, 0.000000000000000000, 1.000000000000000000 ) ) ;
#6700=VECTOR ( 'NONE', #42161, 1000.000000000000000 ) ;
#6708=ORIENTED_EDGE ( 'NONE', *, *, #2932, .F. ) ;
#6777=ORIENTED_EDGE ( 'NONE', *, *, #28846, .F. ) ;
#6813=ADVANCED_FACE ( 'NONE', ( #14750 ), #22571, .F. ) ;
#6847=ORIENTED_EDGE ( 'NONE', *, *, #30448, .T. ) ;
#6865=EDGE_CURVE ( 'NONE', #6291, #17248, #19367, .T. ) ;
#6935=CARTESIAN_POINT ( 'NONE',  ( 1.250000000000000444, -16.78109714094927085, -1.199999999999999956 ) ) ;
#7037=ORIENTED_EDGE ( 'NONE', *, *, #14144, .T. ) ;
#7206=CARTESIAN_POINT ( 'NONE',  ( 1.250000000000000444, -16.78109714094927085, -1.199999999999999956 ) ) ;
#7270=CIRCLE ( 'NONE', #14294, 11.59999999999999964 ) ;
#7313=VECTOR ( 'NONE', #20159, 1000.000000000000000 ) ;
#7372=CARTESIAN_POINT ( 'NONE',  ( -7.001685179585692254, -14.98378029539707512, -1.199999999999999956 ) ) ;
#7421=EDGE_CURVE ( 'NONE', #28409, #6291, #16858, .T. ) ;
#7445=ORIENTED_EDGE ( 'NONE', *, *, #38046, .T. ) ;
#7452=ORIENTED_EDGE ( 'NONE', *, *, #3127, .T. ) ;
#7467=CARTESIAN_POINT ( 'NONE',  ( -11.59999999999999964, -0.8299999999999986278, -1.199999999999999956 ) ) ;
#7668=VERTEX_POINT ( 'NONE', #38313 ) ;
#7696=LINE ( 'NONE', #33634, #12782 ) ;
#7697=DIRECTION ( 'NONE',  ( 0.000000000000000000, 0.000000000000000000, 1.000000000000000000 ) ) ;
#7708=VERTEX_POINT ( 'NONE', #8679 ) ;
#7864=FACE_OUTER_BOUND ( 'NONE', #23863, .T. ) ;
#7911=CYLINDRICAL_SURFACE ( 'NONE', #9943, 14.09999999999999964 ) ;
#7930=DIRECTION ( 'NONE',  ( -0.000000000000000000, 0.000000000000000000, -1.000000000000000000 ) ) ;
#7946=EDGE_CURVE ( 'NONE', #36155, #15680, #3052, .T. ) ;
#7950=CYLINDRICAL_SURFACE ( 'NONE', #18349, 14.09999999999999964 ) ;
#8045=CARTESIAN_POINT ( 'NONE',  ( -6.719258119307966126, -15.35072898742050462, -1.199999999999999956 ) ) ;
#8060=UNCERTAINTY_MEASURE_WITH_UNIT (LENGTH_MEASURE( 1.000000000000000082E-05 ), #31007, 'distance_accuracy_value', 'NONE');
#8083=ORIENTED_EDGE ( 'NONE', *, *, #19126, .F. ) ;
#8094=ORIENTED_EDGE ( 'NONE', *, *, #22520, .F. ) ;
#8161=DIRECTION ( 'NONE',  ( 1.000000000000000000, 0.000000000000000000, 0.000000000000000000 ) ) ;
#8231=ORIENTED_EDGE ( 'NONE', *, *, #4630, .F. ) ;
#8368=DIRECTION ( 'NONE',  ( -0.000000000000000000, -0.000000000000000000, -1.000000000000000000 ) ) ;
#8390=ORIENTED_EDGE ( 'NONE', *, *, #44215, .F. ) ;
#8488=VECTOR ( 'NONE', #26494, 1000.000000000000000 ) ;
#8518=DIRECTION ( 'NONE',  ( 1.000000000000000000, 0.000000000000000000, 0.000000000000000000 ) ) ;
#8535=CARTESIAN_POINT ( 'NONE',  ( 7.001685179585692254, -14.98378029539707512, -1.199999999999999956 ) ) ;
#8551=ORIENTED_EDGE ( 'NONE', *, *, #26783, .F. ) ;
#8610=EDGE_CURVE ( 'NONE', #31655, #11482, #12613, .T. ) ;
#8679=CARTESIAN_POINT ( 'NONE',  ( 6.719258119307965238, -15.35072898742050107, -1.199999999999999956 ) ) ;
#8681=EDGE_CURVE ( 'NONE', #12258, #441, #34285, .T. ) ;
#8949=EDGE_CURVE ( 'NONE', #4532, #41636, #44396, .T. ) ;
#8975=PRESENTATION_STYLE_ASSIGNMENT (( #20462 ) ) ;
#9184=ORIENTED_EDGE ( 'NONE', *, *, #48290, .F. ) ;
#9214=PRODUCT_CONTEXT ( 'NONE', #41030, 'mechanical' ) ;
#9263=CARTESIAN_POINT ( 'NONE',  ( 0.000000000000000000, -0.8299999999999999600, -1.199999999999999956 ) ) ;
#9319=DIRECTION ( 'NONE',  ( 0.1736481776669309418, 0.9848077530122080203, -0.000000000000000000 ) ) ;
#9343=ORIENTED_EDGE ( 'NONE', *, *, #7421, .F. ) ;
#9378=DIRECTION ( 'NONE',  ( 0.000000000000000000, 0.000000000000000000, 1.000000000000000000 ) ) ;
#9423=( NAMED_UNIT ( * ) PLANE_ANGLE_UNIT ( ) SI_UNIT ( $, .RADIAN. ) );
#9456=CARTESIAN_POINT ( 'NONE',  ( -3.249999999999999556, -13.95926121303099343, -1.199999999999999956 ) ) ;
#9466=ORIENTED_EDGE ( 'NONE', *, *, #8681, .T. ) ;
#9601=CARTESIAN_POINT ( 'NONE',  ( 0.000000000000000000, -0.8299999999999999600, -1.199999999999999956 ) ) ;
#9620=AXIS2_PLACEMENT_3D ( 'NONE', #39003, #35571, #16728 ) ;
#9639=CARTESIAN_POINT ( 'NONE',  ( 0.000000000000000000, -0.8299999999999999600, -1.199999999999999956 ) ) ;
#9751=CARTESIAN_POINT ( 'NONE',  ( -8.452893869119503023, -12.51233732111638375, 0.000000000000000000 ) ) ;
#9856=VERTEX_POINT ( 'NONE', #29768 ) ;
#9858=VECTOR ( 'NONE', #7697, 1000.000000000000000 ) ;
#9875=AXIS2_PLACEMENT_3D ( 'NONE', #13157, #6297, #46451 ) ;
#9935=LINE ( 'NONE', #13602, #37040 ) ;
#9943=AXIS2_PLACEMENT_3D ( 'NONE', #27254, #37775, #8161 ) ;
#9960=AXIS2_PLACEMENT_3D ( 'NONE', #32097, #34595, #2455 ) ;
#10112=ORIENTED_EDGE ( 'NONE', *, *, #7946, .F. ) ;
#10133=EDGE_LOOP ( 'NONE', ( #20923, #47742, #26447, #24480 ) ) ;
#10238=DIRECTION ( 'NONE',  ( -0.000000000000000000, -0.000000000000000000, -1.000000000000000000 ) ) ;
#10354=CIRCLE ( 'NONE', #42396, 0.5000000000000004441 ) ;
#10381=VERTEX_POINT ( 'NONE', #27753 ) ;
#10393=DIRECTION ( 'NONE',  ( 1.000000000000000000, 0.000000000000000000, 0.000000000000000000 ) ) ;
#10582=ORIENTED_EDGE ( 'NONE', *, *, #36569, .T. ) ;
#10632=AXIS2_PLACEMENT_3D ( 'NONE', #18939, #7930, #34123 ) ;
#10659=LINE ( 'NONE', #21893, #7313 ) ;
#10710=CARTESIAN_POINT ( 'NONE',  ( 5.250000000000000000, -13.95926121303099343, 0.000000000000000000 ) ) ;
#10766=CARTESIAN_POINT ( 'NONE',  ( -6.509281303079589520, -14.89695620656361008, -1.199999999999999956 ) ) ;
#10778=CYLINDRICAL_SURFACE ( 'NONE', #13119, 11.59999999999999964 ) ;
#10815=DIRECTION ( 'NONE',  ( 1.000000000000000000, 0.000000000000000000, 0.000000000000000000 ) ) ;
#10875=DIRECTION ( 'NONE',  ( 0.000000000000000000, 0.000000000000000000, 1.000000000000000000 ) ) ;
#10881=CARTESIAN_POINT ( 'NONE',  ( 6.719258119307966126, -15.35072898742050462, -1.199999999999999956 ) ) ;
#11028=VERTEX_POINT ( 'NONE', #39428 ) ;
#11051=VECTOR ( 'NONE', #30260, 1000.000000000000000 ) ;
#11068=ORIENTED_EDGE ( 'NONE', *, *, #26783, .T. ) ;
#11153=AXIS2_PLACEMENT_3D ( 'NONE', #28003, #9378, #31440 ) ;
#11165=ORIENTED_EDGE ( 'NONE', *, *, #22555, .F. ) ;
#11270=CIRCLE ( 'NONE', #2648, 11.59999999999999964 ) ;
#11414=CARTESIAN_POINT ( 'NONE',  ( 0.000000000000000000, 0.000000000000000000, -1.199999999999999956 ) ) ;
#11482=VERTEX_POINT ( 'NONE', #41242 ) ;
#11586=LINE ( 'NONE', #26515, #6700 ) ;
#11636=AXIS2_PLACEMENT_3D ( 'NONE', #13959, #6619, #3667 ) ;
#11646=CARTESIAN_POINT ( 'NONE',  ( -7.001685179585692254, -14.98378029539707512, -1.199999999999999956 ) ) ;
#11655=CIRCLE ( 'NONE', #39020, 0.5000000000000004441 ) ;
#11675=CARTESIAN_POINT ( 'NONE',  ( 8.452893869119503023, -12.51233732111638375, 0.000000000000000000 ) ) ;
#11707=ORIENTED_EDGE ( 'NONE', *, *, #17551, .F. ) ;
#11761=AXIS2_PLACEMENT_3D ( 'NONE', #21164, #35857, #6021 ) ;
#11956=EDGE_LOOP ( 'NONE', ( #15607, #27327, #38008, #9466, #2950, #9343, #23736, #1903, #44795, #10582, #8551, #34313, #19596, #44265, #892, #9184 ) ) ;
#12053=CARTESIAN_POINT ( 'NONE',  ( 0.000000000000000000, -0.8299999999999999600, 0.000000000000000000 ) ) ;
#12072=EDGE_LOOP ( 'NONE', ( #41112, #43962, #8231, #7445 ) ) ;
#12115=ORIENTED_EDGE ( 'NONE', *, *, #22979, .T. ) ;
#12124=EDGE_CURVE ( 'NONE', #47625, #19393, #38958, .T. ) ;
#12181=DIRECTION ( 'NONE',  ( 9.814797785686868941E-17, -1.000000000000000000, 0.000000000000000000 ) ) ;
#12258=VERTEX_POINT ( 'NONE', #19259 ) ;
#12328=FACE_OUTER_BOUND ( 'NONE', #29013, .T. ) ;
#12375=( GEOMETRIC_REPRESENTATION_CONTEXT ( 3 ) GLOBAL_UNCERTAINTY_ASSIGNED_CONTEXT ( ( #33523 ) ) GLOBAL_UNIT_ASSIGNED_CONTEXT ( ( #40232, #31759, #28065 ) ) REPRESENTATION_CONTEXT ( 'NONE', 'WORKASPACE' ) );
#12377=CARTESIAN_POINT ( 'NONE',  ( 1.250000000000000000, -12.36245420541525597, -1.199999999999999956 ) ) ;
#12407=VECTOR ( 'NONE', #31466, 1000.000000000000000 ) ;
#12412=EDGE_CURVE ( 'NONE', #10381, #47625, #9935, .T. ) ;
#12426=AXIS2_PLACEMENT_3D ( 'NONE', #32050, #23720, #31089 ) ;
#12444=EDGE_CURVE ( 'NONE', #25916, #11028, #11270, .T. ) ;
#12462=DIRECTION ( 'NONE',  ( 0.000000000000000000, 0.000000000000000000, 1.000000000000000000 ) ) ;
#12481=ORIENTED_EDGE ( 'NONE', *, *, #45645, .T. ) ;
#12528=CARTESIAN_POINT ( 'NONE',  ( -1.250000000000000000, -12.36245420541525597, -1.199999999999999956 ) ) ;
#12593=AXIS2_PLACEMENT_3D ( 'NONE', #41412, #14744, #3474 ) ;
#12596=CIRCLE ( 'NONE', #47721, 1.000000000000000888 ) ;
#12613=LINE ( 'NONE', #12377, #12407 ) ;
#12623=CARTESIAN_POINT ( 'NONE',  ( -11.59999999999999964, -0.8299999999999986278, -1.199999999999999956 ) ) ;
#12642=CARTESIAN_POINT ( 'NONE',  ( -5.250000000000000888, -13.95926121303099343, -1.199999999999999956 ) ) ;
#12703=FACE_OUTER_BOUND ( 'NONE', #33360, .T. ) ;
#12782=VECTOR ( 'NONE', #100, 1000.000000000000000 ) ;
#12910=LINE ( 'NONE', #9456, #45268 ) ;
#13091=PLANE ( 'NONE',  #4337 ) ;
#13119=AXIS2_PLACEMENT_3D ( 'NONE', #17629, #36942, #37200 ) ;
#13129=AXIS2_PLACEMENT_3D ( 'NONE', #36270, #3207, #10815 ) ;
#13141=DIRECTION ( 'NONE',  ( 0.000000000000000000, 0.000000000000000000, 1.000000000000000000 ) ) ;
#13157=CARTESIAN_POINT ( 'NONE',  ( 7.543218489614351263, -11.91259227951415056, -1.199999999999999956 ) ) ;
#13432=CIRCLE ( 'NONE', #23587, 1.000000000000000000 ) ;
#13567=ORIENTED_EDGE ( 'NONE', *, *, #36413, .F. ) ;
#13602=CARTESIAN_POINT ( 'NONE',  ( 7.001685179585692254, -14.98378029539707512, -1.199999999999999956 ) ) ;
#13627=EDGE_LOOP ( 'NONE', ( #18260, #8094, #40228, #5398 ) ) ;
#13662=CARTESIAN_POINT ( 'NONE',  ( -14.09999999999999964, 1.726751986797767995E-15, -1.199999999999999956 ) ) ;
#13680=VECTOR ( 'NONE', #4018, 1000.000000000000000 ) ;
#13740=CIRCLE ( 'NONE', #39528, 1.000000000000000888 ) ;
#13818=EDGE_CURVE ( 'NONE', #18357, #1286, #26823, .T. ) ;
#13851=CARTESIAN_POINT ( 'NONE',  ( 14.09999999999999964, 0.000000000000000000, 0.000000000000000000 ) ) ;
#13913=DIRECTION ( 'NONE',  ( -1.000000000000000000, 0.000000000000000000, 0.000000000000000000 ) ) ;
#13921=ORIENTED_EDGE ( 'NONE', *, *, #42208, .F. ) ;
#13959=CARTESIAN_POINT ( 'NONE',  ( 0.000000000000000000, 0.000000000000000000, 0.000000000000000000 ) ) ;
#13968=ORIENTED_EDGE ( 'NONE', *, *, #15467, .F. ) ;
#13976=EDGE_LOOP ( 'NONE', ( #1952, #12481, #30339, #29946 ) ) ;
#14066=CARTESIAN_POINT ( 'NONE',  ( 11.59999999999999964, -0.8299999999999999600, 0.000000000000000000 ) ) ;
#14068=MECHANICAL_DESIGN_GEOMETRIC_PRESENTATION_REPRESENTATION('',(#31273),#22652);
#14107=ORIENTED_EDGE ( 'NONE', *, *, #47145, .T. ) ;
#14139=DIRECTION ( 'NONE',  ( 0.000000000000000000, 0.000000000000000000, 1.000000000000000000 ) ) ;
#14144=EDGE_CURVE ( 'NONE', #10381, #25961, #40476, .T. ) ;
#14187=ORIENTED_EDGE ( 'NONE', *, *, #15197, .T. ) ;
#14294=AXIS2_PLACEMENT_3D ( 'NONE', #12053, #8368, #4929 ) ;
#14316=CIRCLE ( 'NONE', #45573, 11.59999999999999964 ) ;
#14317=FACE_OUTER_BOUND ( 'NONE', #24570, .T. ) ;
#14423=CARTESIAN_POINT ( 'NONE',  ( 6.509281303079589520, -14.89695620656361008, 0.000000000000000000 ) ) ;
#14526=DIRECTION ( 'NONE',  ( 0.1736481776669309418, 0.9848077530122080203, -0.000000000000000000 ) ) ;
#14560=CARTESIAN_POINT ( 'NONE',  ( -1.250000000000002442, -12.36245420541525242, -1.199999999999999956 ) ) ;
#14683=DIRECTION ( 'NONE',  ( 0.000000000000000000, 0.000000000000000000, 1.000000000000000000 ) ) ;
#14744=DIRECTION ( 'NONE',  ( 0.000000000000000000, 0.000000000000000000, 1.000000000000000000 ) ) ;
#14750=FACE_OUTER_BOUND ( 'NONE', #39813, .T. ) ;
#14975=CIRCLE ( 'NONE', #45435, 14.09999999999999964 ) ;
#14990=CARTESIAN_POINT ( 'NONE',  ( 0.000000000000000000, -0.8299999999999999600, 0.000000000000000000 ) ) ;
#15061=AXIS2_PLACEMENT_3D ( 'NONE', #6603, #18581, #17609 ) ;
#15095=CARTESIAN_POINT ( 'NONE',  ( 0.000000000000000000, -0.8299999999999999600, -1.199999999999999956 ) ) ;
#15175=LINE ( 'NONE', #30101, #16925 ) ;
#15197=EDGE_CURVE ( 'NONE', #31943, #25264, #30045, .T. ) ;
#15309=DIRECTION ( 'NONE',  ( 1.000000000000000000, 0.000000000000000000, 0.000000000000000000 ) ) ;
#15348=DIRECTION ( 'NONE',  ( 1.000000000000000000, 0.000000000000000000, 0.000000000000000000 ) ) ;
#15467=EDGE_CURVE ( 'NONE', #45354, #7668, #18432, .T. ) ;
#15476=DIRECTION ( 'NONE',  ( -1.000000000000000000, 0.000000000000000000, 0.000000000000000000 ) ) ;
#15576=PLANE ( 'NONE',  #31705 ) ;
#15607=ORIENTED_EDGE ( 'NONE', *, *, #34839, .F. ) ;
#15653=DIRECTION ( 'NONE',  ( 1.000000000000000000, 0.000000000000000000, 0.000000000000000000 ) ) ;
#15680=VERTEX_POINT ( 'NONE', #32353 ) ;
#15880=ORIENTED_EDGE ( 'NONE', *, *, #12124, .T. ) ;
#15904=AXIS2_PLACEMENT_3D ( 'NONE', #9751, #35457, #17093 ) ;
#15954=ORIENTED_EDGE ( 'NONE', *, *, #12412, .T. ) ;
#15955=AXIS2_PLACEMENT_3D ( 'NONE', #9601, #47310, #17425 ) ;
#16094=( NAMED_UNIT ( * ) SI_UNIT ( $, .STERADIAN. ) SOLID_ANGLE_UNIT ( ) );
#16155=DIRECTION ( 'NONE',  ( 0.000000000000000000, 0.000000000000000000, 1.000000000000000000 ) ) ;
#16300=DIRECTION ( 'NONE',  ( 0.000000000000000000, 0.000000000000000000, 1.000000000000000000 ) ) ;
#16453=ORIENTED_EDGE ( 'NONE', *, *, #17551, .T. ) ;
#16559=( LENGTH_UNIT ( ) NAMED_UNIT ( * ) SI_UNIT ( .MILLI., .METRE. ) );
#16653=CIRCLE ( 'NONE', #9620, 16.00000000000000000 ) ;
#16678=CIRCLE ( 'NONE', #15904, 0.9999999999999991118 ) ;
#16728=DIRECTION ( 'NONE',  ( -1.000000000000000000, 0.000000000000000000, 0.000000000000000000 ) ) ;
#16749=ADVANCED_FACE ( 'NONE', ( #5744, #46862, #21136 ), #13091, .T. ) ;
#16804=CARTESIAN_POINT ( 'NONE',  ( 0.000000000000000000, -0.8299999999999999600, 0.000000000000000000 ) ) ;
#16858=CIRCLE ( 'NONE', #2012, 14.09999999999999964 ) ;
#16864=CARTESIAN_POINT ( 'NONE',  ( 4.250000000000000000, -13.95926121303099343, -1.199999999999999956 ) ) ;
#16866=CARTESIAN_POINT ( 'NONE',  ( 0.000000000000000000, 0.000000000000000000, -1.199999999999999956 ) ) ;
#16898=CARTESIAN_POINT ( 'NONE',  ( 7.468086116107294004, -12.33868914344945189, 0.000000000000000000 ) ) ;
#16925=VECTOR ( 'NONE', #941, 1000.000000000000114 ) ;
#17076=EDGE_CURVE ( 'NONE', #24143, #25916, #11586, .T. ) ;
#17093=DIRECTION ( 'NONE',  ( -1.000000000000000000, 0.000000000000000000, 0.000000000000000000 ) ) ;
#17104=AXIS2_PLACEMENT_3D ( 'NONE', #33846, #23086, #26521 ) ;
#17148=CYLINDRICAL_SURFACE ( 'NONE', #9960, 16.00000000000000000 ) ;
#17154=VERTEX_POINT ( 'NONE', #32124 ) ;
#17248=VERTEX_POINT ( 'NONE', #38984 ) ;
#17272=DIRECTION ( 'NONE',  ( -0.000000000000000000, -0.000000000000000000, -1.000000000000000000 ) ) ;
#17290=VERTEX_POINT ( 'NONE', #17885 ) ;
#17308=AXIS2_PLACEMENT_3D ( 'NONE', #23740, #28141, #46988 ) ;
#17362=VECTOR ( 'NONE', #38200, 1000.000000000000000 ) ;
#17425=DIRECTION ( 'NONE',  ( 1.000000000000000000, 0.000000000000000000, 0.000000000000000000 ) ) ;
#17532=AXIS2_PLACEMENT_3D ( 'NONE', #14990, #12462, #37256 ) ;
#17551=EDGE_CURVE ( 'NONE', #47247, #20870, #21986, .T. ) ;
#17591=CARTESIAN_POINT ( 'NONE',  ( -4.250000000000000000, -13.95926121303099343, 0.000000000000000000 ) ) ;
#17609=DIRECTION ( 'NONE',  ( 1.000000000000000000, 0.000000000000000000, 0.000000000000000000 ) ) ;
#17629=CARTESIAN_POINT ( 'NONE',  ( 0.000000000000000000, -0.8299999999999999600, -1.199999999999999956 ) ) ;
#17663=LINE ( 'NONE', #32596, #32079 ) ;
#17717=EDGE_LOOP ( 'NONE', ( #23301, #3414, #31840, #6847, #1547, #34435, #7452, #5316, #5776, #21602, #14107, #32789, #35955, #44448, #7037, #28917 ) ) ;
#17885=CARTESIAN_POINT ( 'NONE',  ( 6.719258119307965238, -15.35072898742050107, 0.000000000000000000 ) ) ;
#17985=AXIS2_PLACEMENT_3D ( 'NONE', #33900, #26570, #37826 ) ;
#18012=ORIENTED_EDGE ( 'NONE', *, *, #29938, .F. ) ;
#18040=AXIS2_PLACEMENT_3D ( 'NONE', #41828, #38151, #8518 ) ;
#18124=CARTESIAN_POINT ( 'NONE',  ( -6.719258119307965238, -15.35072898742050107, 0.000000000000000000 ) ) ;
#18260=ORIENTED_EDGE ( 'NONE', *, *, #17076, .F. ) ;
#18349=AXIS2_PLACEMENT_3D ( 'NONE', #11414, #41263, #45397 ) ;
#18357=VERTEX_POINT ( 'NONE', #24290 ) ;
#18432=LINE ( 'NONE', #6935, #4183 ) ;
#18453=CARTESIAN_POINT ( 'NONE',  ( 3.250000000000000444, -13.95926121303099343, -1.199999999999999956 ) ) ;
#18492=CARTESIAN_POINT ( 'NONE',  ( 0.000000000000000000, 0.000000000000000000, -1.199999999999999956 ) ) ;
#18581=DIRECTION ( 'NONE',  ( 0.000000000000000000, 0.000000000000000000, 1.000000000000000000 ) ) ;
#18602=EDGE_CURVE ( 'NONE', #441, #25278, #17663, .T. ) ;
#18811=CARTESIAN_POINT ( 'NONE',  ( 11.59999999999999964, -0.8299999999999999600, -1.199999999999999956 ) ) ;
#18824=CIRCLE ( 'NONE', #12593, 1.000000000000000000 ) ;
#18841=ORIENTED_EDGE ( 'NONE', *, *, #453, .F. ) ;
#18920=LINE ( 'NONE', #27023, #13680 ) ;
#18939=CARTESIAN_POINT ( 'NONE',  ( 0.000000000000000000, -0.8299999999999999600, 0.000000000000000000 ) ) ;
#18988=SURFACE_STYLE_USAGE ( .BOTH. , #41055 ) ;
#19126=EDGE_CURVE ( 'NONE', #22374, #28331, #35233, .T. ) ;
#19151=VECTOR ( 'NONE', #10875, 1000.000000000000000 ) ;
#19166=CARTESIAN_POINT ( 'NONE',  ( -7.543218489614351263, -11.91259227951415056, 0.000000000000000000 ) ) ;
#19242=CYLINDRICAL_SURFACE ( 'NONE', #42461, 16.00000000000000000 ) ;
#19259=CARTESIAN_POINT ( 'NONE',  ( -7.468086116107294004, -12.33868914344945189, -1.199999999999999956 ) ) ;
#19267=CARTESIAN_POINT ( 'NONE',  ( 4.250000000000000000, -13.95926121303099343, -1.199999999999999956 ) ) ;
#19325=AXIS2_PLACEMENT_3D ( 'NONE', #44178, #24850, #40741 ) ;
#19326=ORIENTED_EDGE ( 'NONE', *, *, #15467, .T. ) ;
#19367=LINE ( 'NONE', #29909, #24705 ) ;
#19393=VERTEX_POINT ( 'NONE', #39841 ) ;
#19422=FACE_BOUND ( 'NONE', #25719, .T. ) ;
#19453=AXIS2_PLACEMENT_3D ( 'NONE', #44016, #10238, #25887 ) ;
#19474=DIRECTION ( 'NONE',  ( -0.000000000000000000, -0.000000000000000000, -1.000000000000000000 ) ) ;
#19492=DIRECTION ( 'NONE',  ( 0.000000000000000000, 0.000000000000000000, 1.000000000000000000 ) ) ;
#19494=MANIFOLD_SOLID_BREP ( 'Fillet2', #41908 ) ;
#19596=ORIENTED_EDGE ( 'NONE', *, *, #26584, .F. ) ;
#19663=FACE_OUTER_BOUND ( 'NONE', #30505, .T. ) ;
#19673=EDGE_CURVE ( 'NONE', #41636, #199, #27390, .T. ) ;
#19748=CARTESIAN_POINT ( 'NONE',  ( -7.543218489614351263, -11.91259227951415056, -1.199999999999999956 ) ) ;
#20159=DIRECTION ( 'NONE',  ( 0.000000000000000000, 0.000000000000000000, 1.000000000000000000 ) ) ;
#20183=DIRECTION ( 'NONE',  ( -1.000000000000000000, 0.000000000000000000, 0.000000000000000000 ) ) ;
#20462=SURFACE_STYLE_USAGE ( .BOTH. , #35150 ) ;
#20517=DIRECTION ( 'NONE',  ( 1.000000000000000000, 0.000000000000000000, 0.000000000000000000 ) ) ;
#20870=VERTEX_POINT ( 'NONE', #10710 ) ;
#20923=ORIENTED_EDGE ( 'NONE', *, *, #3127, .F. ) ;
#21136=FACE_OUTER_BOUND ( 'NONE', #11956, .T. ) ;
#21164=CARTESIAN_POINT ( 'NONE',  ( -6.509281303079589520, -14.89695620656361008, 0.000000000000000000 ) ) ;
#21223=SHAPE_REPRESENTATION ( 'CIRCLIP DIN 471 - 25 \X2\00d7\X0\ 1.2_GB_CONNECTING_PIECE_RING_RRA 25', ( #11636 ), #12375 ) ;
#21228=DIRECTION ( 'NONE',  ( 9.814797785686868941E-17, -1.000000000000000000, 0.000000000000000000 ) ) ;
#21437=CARTESIAN_POINT ( 'NONE',  ( 6.509281303079589520, -14.89695620656361008, -1.199999999999999956 ) ) ;
#21482=LINE ( 'NONE', #32505, #43240 ) ;
#21564=EDGE_CURVE ( 'NONE', #199, #9856, #41357, .T. ) ;
#21602=ORIENTED_EDGE ( 'NONE', *, *, #29938, .T. ) ;
#21751=COLOUR_RGB ( '', 0.09019608, 0.27058824, 0.51372549) ;
#21852=DIRECTION ( 'NONE',  ( 0.000000000000000000, 0.000000000000000000, 1.000000000000000000 ) ) ;
#21893=CARTESIAN_POINT ( 'NONE',  ( 11.59999999999999964, -0.8299999999999999600, -1.199999999999999956 ) ) ;
#21900=EDGE_CURVE ( 'NONE', #31943, #20870, #21482, .T. ) ;
#21902=ORIENTED_EDGE ( 'NONE', *, *, #44357, .T. ) ;
#21986=CIRCLE ( 'NONE', #17308, 1.000000000000000000 ) ;
#22195=EDGE_CURVE ( 'NONE', #28331, #15680, #37859, .T. ) ;
#22273=VECTOR ( 'NONE', #29477, 1000.000000000000000 ) ;
#22374=VERTEX_POINT ( 'NONE', #32211 ) ;
#22413=CYLINDRICAL_SURFACE ( 'NONE', #23420, 14.09999999999999964 ) ;
#22520=EDGE_CURVE ( 'NONE', #17154, #24143, #7696, .T. ) ;
#22555=EDGE_CURVE ( 'NONE', #6051, #43074, #10659, .T. ) ;
#22571=CYLINDRICAL_SURFACE ( 'NONE', #30976, 0.9999999999999991118 ) ;
#22582=ORIENTED_EDGE ( 'NONE', *, *, #18602, .F. ) ;
#22652=( GEOMETRIC_REPRESENTATION_CONTEXT ( 3 ) GLOBAL_UNCERTAINTY_ASSIGNED_CONTEXT ( ( #8060 ) ) GLOBAL_UNIT_ASSIGNED_CONTEXT ( ( #31007, #9423, #45926 ) ) REPRESENTATION_CONTEXT ( 'NONE', 'WORKASPACE' ) );
#22956=ORIENTED_EDGE ( 'NONE', *, *, #27770, .F. ) ;
#22979=EDGE_CURVE ( 'NONE', #20870, #47247, #33139, .T. ) ;
#23086=DIRECTION ( 'NONE',  ( 0.000000000000000000, 0.000000000000000000, 1.000000000000000000 ) ) ;
#23301=ORIENTED_EDGE ( 'NONE', *, *, #4630, .T. ) ;
#23305=PRODUCT_DEFINITION_FORMATION_WITH_SPECIFIED_SOURCE ( 'ANY', '', #1883, .NOT_KNOWN. ) ;
#23355=ORIENTED_EDGE ( 'NONE', *, *, #37401, .F. ) ;
#23378=LINE ( 'NONE', #4547, #11051 ) ;
#23420=AXIS2_PLACEMENT_3D ( 'NONE', #18492, #41261, #26326 ) ;
#23527=DIRECTION ( 'NONE',  ( 0.000000000000000000, 0.000000000000000000, 1.000000000000000000 ) ) ;
#23587=AXIS2_PLACEMENT_3D ( 'NONE', #11675, #19474, #45438 ) ;
#23643=DIRECTION ( 'NONE',  ( 0.000000000000000000, 0.000000000000000000, 1.000000000000000000 ) ) ;
#23672=AXIS2_PLACEMENT_3D ( 'NONE', #40292, #25575, #15309 ) ;
#23720=DIRECTION ( 'NONE',  ( 0.000000000000000000, 0.000000000000000000, 1.000000000000000000 ) ) ;
#23736=ORIENTED_EDGE ( 'NONE', *, *, #29464, .F. ) ;
#23740=CARTESIAN_POINT ( 'NONE',  ( 4.250000000000000000, -13.95926121303099343, 0.000000000000000000 ) ) ;
#23756=CARTESIAN_POINT ( 'NONE',  ( 0.000000000000000000, -0.8299999999999999600, -1.199999999999999956 ) ) ;
#23863=EDGE_LOOP ( 'NONE', ( #6708, #45515, #34859, #13567 ) ) ;
#23868=DIRECTION ( 'NONE',  ( 0.000000000000000000, 0.000000000000000000, 1.000000000000000000 ) ) ;
#23910=SHAPE_REPRESENTATION_RELATIONSHIP ( 'NONE' , 'NONE' ,  #21223, #27490 ) ;
#24066=FACE_OUTER_BOUND ( 'NONE', #36111, .T. ) ;
#24143=VERTEX_POINT ( 'NONE', #27663 ) ;
#24147=FILL_AREA_STYLE ('',( #5313 ) ) ;
#24215=ORIENTED_EDGE ( 'NONE', *, *, #8681, .F. ) ;
#24229=COLOUR_RGB ( '', 0.09019608, 0.27058824, 0.51372549) ;
#24238=FACE_OUTER_BOUND ( 'NONE', #48254, .T. ) ;
#24284=FACE_OUTER_BOUND ( 'NONE', #13627, .T. ) ;
#24290=CARTESIAN_POINT ( 'NONE',  ( -1.250000000000002442, -12.36245420541525242, -1.199999999999999956 ) ) ;
#24292=AXIS2_PLACEMENT_3D ( 'NONE', #41329, #26630, #4839 ) ;
#24442=PRODUCT_DEFINITION ( 'UNKNOWN', '', #23305, #3173 ) ;
#24478=CARTESIAN_POINT ( 'NONE',  ( -1.250000000000002442, -12.36245420541525242, 0.000000000000000000 ) ) ;
#24480=ORIENTED_EDGE ( 'NONE', *, *, #22520, .T. ) ;
#24529=DIRECTION ( 'NONE',  ( 1.000000000000000000, -9.814797785686868941E-17, 0.000000000000000000 ) ) ;
#24570=EDGE_LOOP ( 'NONE', ( #43570, #8083, #39620, #42246 ) ) ;
#24622=ADVANCED_FACE ( 'NONE', ( #37898 ), #41571, .T. ) ;
#24626=DIRECTION ( 'NONE',  ( -0.000000000000000000, -0.000000000000000000, -1.000000000000000000 ) ) ;
#24705=VECTOR ( 'NONE', #26250, 1000.000000000000000 ) ;
#24722=DIRECTION ( 'NONE',  ( 0.000000000000000000, 0.000000000000000000, 1.000000000000000000 ) ) ;
#24753=ADVANCED_FACE ( 'NONE', ( #39341 ), #43738, .T. ) ;
#24850=DIRECTION ( 'NONE',  ( 0.000000000000000000, 0.000000000000000000, 1.000000000000000000 ) ) ;
#25020=CARTESIAN_POINT ( 'NONE',  ( -5.250000000000000888, -13.95926121303099343, -1.199999999999999956 ) ) ;
#25264=VERTEX_POINT ( 'NONE', #18453 ) ;
#25278=VERTEX_POINT ( 'NONE', #40495 ) ;
#25428=ORIENTED_EDGE ( 'NONE', *, *, #453, .T. ) ;
#25436=ORIENTED_EDGE ( 'NONE', *, *, #39233, .F. ) ;
#25509=DIRECTION ( 'NONE',  ( 0.000000000000000000, 0.000000000000000000, 1.000000000000000000 ) ) ;
#25519=ADVANCED_FACE ( 'NONE', ( #12328 ), #7911, .T. ) ;
#25572=ORIENTED_EDGE ( 'NONE', *, *, #28028, .F. ) ;
#25575=DIRECTION ( 'NONE',  ( -0.000000000000000000, -0.000000000000000000, -1.000000000000000000 ) ) ;
#25643=ADVANCED_FACE ( 'NONE', ( #24066 ), #38994, .T. ) ;
#25683=FACE_OUTER_BOUND ( 'NONE', #38927, .T. ) ;
#25719=EDGE_LOOP ( 'NONE', ( #27742, #11707 ) ) ;
#25816=AXIS2_PLACEMENT_3D ( 'NONE', #1372, #16300, #2800 ) ;
#25851=VECTOR ( 'NONE', #45141, 1000.000000000000000 ) ;
#25887=DIRECTION ( 'NONE',  ( -1.000000000000000000, 0.000000000000000000, 0.000000000000000000 ) ) ;
#25916=VERTEX_POINT ( 'NONE', #24478 ) ;
#25961=VERTEX_POINT ( 'NONE', #16898 ) ;
#26241=DIRECTION ( 'NONE',  ( 1.000000000000000000, 0.000000000000000000, 0.000000000000000000 ) ) ;
#26250=DIRECTION ( 'NONE',  ( 0.000000000000000000, 0.000000000000000000, 1.000000000000000000 ) ) ;
#26326=DIRECTION ( 'NONE',  ( 1.000000000000000000, 0.000000000000000000, 0.000000000000000000 ) ) ;
#26447=ORIENTED_EDGE ( 'NONE', *, *, #34839, .T. ) ;
#26494=DIRECTION ( 'NONE',  ( 9.814797785686868941E-17, 1.000000000000000000, -0.000000000000000000 ) ) ;
#26515=CARTESIAN_POINT ( 'NONE',  ( -1.250000000000000000, -12.36245420541525597, 0.000000000000000000 ) ) ;
#26521=DIRECTION ( 'NONE',  ( 1.000000000000000000, 0.000000000000000000, 0.000000000000000000 ) ) ;
#26570=DIRECTION ( 'NONE',  ( 0.000000000000000000, 0.000000000000000000, 1.000000000000000000 ) ) ;
#26584=EDGE_CURVE ( 'NONE', #6051, #31655, #14316, .T. ) ;
#26630=DIRECTION ( 'NONE',  ( 0.000000000000000000, 0.000000000000000000, 1.000000000000000000 ) ) ;
#26783=EDGE_CURVE ( 'NONE', #45354, #7708, #16653, .T. ) ;
#26810=ORIENTED_EDGE ( 'NONE', *, *, #8949, .F. ) ;
#26823=CIRCLE ( 'NONE', #23672, 11.59999999999999964 ) ;
#27023=CARTESIAN_POINT ( 'NONE',  ( -7.468086116107294004, -12.33868914344945189, -1.199999999999999956 ) ) ;
#27107=ADVANCED_FACE ( 'NONE', ( #7864 ), #274, .F. ) ;
#27122=ORIENTED_EDGE ( 'NONE', *, *, #28471, .T. ) ;
#27202=DIRECTION ( 'NONE',  ( 1.000000000000000000, 0.000000000000000000, 0.000000000000000000 ) ) ;
#27254=CARTESIAN_POINT ( 'NONE',  ( 0.000000000000000000, 0.000000000000000000, -1.199999999999999956 ) ) ;
#27327=ORIENTED_EDGE ( 'NONE', *, *, #37401, .T. ) ;
#27377=CIRCLE ( 'NONE', #17985, 1.000000000000000000 ) ;
#27390=CIRCLE ( 'NONE', #11761, 0.5000000000000004441 ) ;
#27431=CARTESIAN_POINT ( 'NONE',  ( -7.893099573151324044, -11.68370571044642503, -1.199999999999999956 ) ) ;
#27434=CARTESIAN_POINT ( 'NONE',  ( -7.468086116107294004, -12.33868914344945189, 0.000000000000000000 ) ) ;
#27490=ADVANCED_BREP_SHAPE_REPRESENTATION ( '', ( #19494, #11636 ), #12375 ) ;
#27663=CARTESIAN_POINT ( 'NONE',  ( -1.250000000000000444, -16.78109714094927085, 0.000000000000000000 ) ) ;
#27742=ORIENTED_EDGE ( 'NONE', *, *, #22979, .F. ) ;
#27753=CARTESIAN_POINT ( 'NONE',  ( 7.001685179585692254, -14.98378029539707512, 0.000000000000000000 ) ) ;
#27770=EDGE_CURVE ( 'NONE', #36144, #19393, #27377, .T. ) ;
#27994=ORIENTED_EDGE ( 'NONE', *, *, #19126, .T. ) ;
#28003=CARTESIAN_POINT ( 'NONE',  ( 0.000000000000000000, 0.000000000000000000, -1.199999999999999956 ) ) ;
#28025=ORIENTED_EDGE ( 'NONE', *, *, #28028, .T. ) ;
#28028=EDGE_CURVE ( 'NONE', #7708, #17290, #33625, .T. ) ;
#28065=( NAMED_UNIT ( * ) SI_UNIT ( $, .STERADIAN. ) SOLID_ANGLE_UNIT ( ) );
#28141=DIRECTION ( 'NONE',  ( 0.000000000000000000, 0.000000000000000000, 1.000000000000000000 ) ) ;
#28156=FACE_OUTER_BOUND ( 'NONE', #37900, .T. ) ;
#28250=ORIENTED_EDGE ( 'NONE', *, *, #36569, .F. ) ;
#28331=VERTEX_POINT ( 'NONE', #25020 ) ;
#28409=VERTEX_POINT ( 'NONE', #43870 ) ;
#28452=CIRCLE ( 'NONE', #15955, 11.59999999999999964 ) ;
#28461=PRODUCT_DEFINITION_SHAPE ( 'NONE', 'NONE',  #24442 ) ;
#28471=EDGE_CURVE ( 'NONE', #25264, #31943, #18824, .T. ) ;
#28542=DIRECTION ( 'NONE',  ( -0.000000000000000000, -0.000000000000000000, -1.000000000000000000 ) ) ;
#28583=VECTOR ( 'NONE', #42602, 1000.000000000000000 ) ;
#28594=CARTESIAN_POINT ( 'NONE',  ( 1.250000000000000000, -12.36245420541525597, 0.000000000000000000 ) ) ;
#28805=EDGE_LOOP ( 'NONE', ( #15880, #31307, #4611, #15954 ) ) ;
#28833=CIRCLE ( 'NONE', #19453, 0.5000000000000004441 ) ;
#28846=EDGE_CURVE ( 'NONE', #25961, #5367, #13432, .T. ) ;
#28865=CARTESIAN_POINT ( 'NONE',  ( 1.250000000000000000, -12.36245420541525597, -1.199999999999999956 ) ) ;
#28917=ORIENTED_EDGE ( 'NONE', *, *, #28846, .T. ) ;
#29013=EDGE_LOOP ( 'NONE', ( #47029, #38943, #38130, #8390 ) ) ;
#29085=EDGE_LOOP ( 'NONE', ( #23355, #30347, #31054, #41087 ) ) ;
#29152=VERTEX_POINT ( 'NONE', #13851 ) ;
#29273=AXIS2_PLACEMENT_3D ( 'NONE', #1458, #34480, #15653 ) ;
#29344=ORIENTED_EDGE ( 'NONE', *, *, #8610, .F. ) ;
#29464=EDGE_CURVE ( 'NONE', #36144, #28409, #5672, .T. ) ;
#29477=DIRECTION ( 'NONE',  ( 0.000000000000000000, 0.000000000000000000, 1.000000000000000000 ) ) ;
#29598=DIRECTION ( 'NONE',  ( 1.000000000000000000, 0.000000000000000000, 0.000000000000000000 ) ) ;
#29605=CIRCLE ( 'NONE', #12426, 14.09999999999999964 ) ;
#29731=DIRECTION ( 'NONE',  ( -0.000000000000000000, -0.000000000000000000, -1.000000000000000000 ) ) ;
#29768=CARTESIAN_POINT ( 'NONE',  ( -6.719258119307965238, -15.35072898742050107, -1.199999999999999956 ) ) ;
#29799=ORIENTED_EDGE ( 'NONE', *, *, #41027, .F. ) ;
#29909=CARTESIAN_POINT ( 'NONE',  ( -14.09999999999999964, 1.726751986797767995E-15, -1.199999999999999956 ) ) ;
#29938=EDGE_CURVE ( 'NONE', #11028, #43074, #7270, .T. ) ;
#29946=ORIENTED_EDGE ( 'NONE', *, *, #4982, .F. ) ;
#29953=CARTESIAN_POINT ( 'NONE',  ( 14.09999999999999964, 0.000000000000000000, -1.199999999999999956 ) ) ;
#29973=FACE_BOUND ( 'NONE', #33792, .T. ) ;
#30045=CIRCLE ( 'NONE', #36297, 1.000000000000000000 ) ;
#30101=CARTESIAN_POINT ( 'NONE',  ( -7.543218489614351263, -11.91259227951415056, -1.199999999999999956 ) ) ;
#30260=DIRECTION ( 'NONE',  ( -0.000000000000000000, -0.000000000000000000, 1.000000000000000000 ) ) ;
#30339=ORIENTED_EDGE ( 'NONE', *, *, #18602, .T. ) ;
#30341=DIRECTION ( 'NONE',  ( -0.000000000000000000, -0.000000000000000000, -1.000000000000000000 ) ) ;
#30347=ORIENTED_EDGE ( 'NONE', *, *, #21564, .F. ) ;
#30380=LINE ( 'NONE', #7372, #17362 ) ;
#30448=EDGE_CURVE ( 'NONE', #25278, #4532, #16678, .T. ) ;
#30477=FACE_OUTER_BOUND ( 'NONE', #13976, .T. ) ;
#30505=EDGE_LOOP ( 'NONE', ( #11068, #28025, #6035, #13968 ) ) ;
#30927=ORIENTED_EDGE ( 'NONE', *, *, #26584, .T. ) ;
#30976=AXIS2_PLACEMENT_3D ( 'NONE', #284, #3972, #33812 ) ;
#30983=CARTESIAN_POINT ( 'NONE',  ( 7.893099573151324044, -11.68370571044642503, -1.199999999999999956 ) ) ;
#31007=( LENGTH_UNIT ( ) NAMED_UNIT ( * ) SI_UNIT ( .MILLI., .METRE. ) );
#31054=ORIENTED_EDGE ( 'NONE', *, *, #19673, .F. ) ;
#31089=DIRECTION ( 'NONE',  ( 1.000000000000000000, 0.000000000000000000, 0.000000000000000000 ) ) ;
#31262=SURFACE_STYLE_FILL_AREA ( #24147 ) ;
#31273=STYLED_ITEM ( 'NONE', ( #33921 ), #19494 ) ;
#31288=DIRECTION ( 'NONE',  ( -0.9848077530122080203, -0.1736481776669309696, 0.000000000000000000 ) ) ;
#31307=ORIENTED_EDGE ( 'NONE', *, *, #39233, .T. ) ;
#31440=DIRECTION ( 'NONE',  ( 1.000000000000000000, 0.000000000000000000, 0.000000000000000000 ) ) ;
#31466=DIRECTION ( 'NONE',  ( 0.000000000000000000, 0.000000000000000000, 1.000000000000000000 ) ) ;
#31520=ADVANCED_FACE ( 'NONE', ( #46009 ), #34976, .F. ) ;
#31559=DIRECTION ( 'NONE',  ( 0.000000000000000000, 0.000000000000000000, 1.000000000000000000 ) ) ;
#31655=VERTEX_POINT ( 'NONE', #45426 ) ;
#31705=AXIS2_PLACEMENT_3D ( 'NONE', #28865, #36458, #3394 ) ;
#31724=CIRCLE ( 'NONE', #40306, 14.09999999999999964 ) ;
#31759=( NAMED_UNIT ( * ) PLANE_ANGLE_UNIT ( ) SI_UNIT ( $, .RADIAN. ) );
#31770=EDGE_LOOP ( 'NONE', ( #26810, #21902, #39778, #44558 ) ) ;
#31840=ORIENTED_EDGE ( 'NONE', *, *, #4982, .T. ) ;
#31943=VERTEX_POINT ( 'NONE', #32665 ) ;
#32050=CARTESIAN_POINT ( 'NONE',  ( 0.000000000000000000, 0.000000000000000000, 0.000000000000000000 ) ) ;
#32079=VECTOR ( 'NONE', #44093, 1000.000000000000000 ) ;
#32097=CARTESIAN_POINT ( 'NONE',  ( 0.000000000000000000, -0.8299999999999999600, -1.199999999999999956 ) ) ;
#32124=CARTESIAN_POINT ( 'NONE',  ( -1.250000000000000444, -16.78109714094927085, -1.199999999999999956 ) ) ;
#32153=DIRECTION ( 'NONE',  ( 1.000000000000000000, 0.000000000000000000, 0.000000000000000000 ) ) ;
#32211=CARTESIAN_POINT ( 'NONE',  ( -3.249999999999999556, -13.95926121303099343, -1.199999999999999956 ) ) ;
#32353=CARTESIAN_POINT ( 'NONE',  ( -5.250000000000000888, -13.95926121303099343, 0.000000000000000000 ) ) ;
#32413=VECTOR ( 'NONE', #34094, 1000.000000000000114 ) ;
#32505=CARTESIAN_POINT ( 'NONE',  ( 5.250000000000000000, -13.95926121303099343, -1.199999999999999956 ) ) ;
#32596=CARTESIAN_POINT ( 'NONE',  ( -7.893099573151324044, -11.68370571044642503, -1.199999999999999956 ) ) ;
#32665=CARTESIAN_POINT ( 'NONE',  ( 5.250000000000000000, -13.95926121303099343, -1.199999999999999956 ) ) ;
#32789=ORIENTED_EDGE ( 'NONE', *, *, #6311, .T. ) ;
#32962=ADVANCED_FACE ( 'NONE', ( #34279 ), #37972, .F. ) ;
#33139=CIRCLE ( 'NONE', #39404, 1.000000000000000000 ) ;
#33149=LINE ( 'NONE', #29953, #22273 ) ;
#33161=CYLINDRICAL_SURFACE ( 'NONE', #19325, 1.000000000000000888 ) ;
#33180=EDGE_LOOP ( 'NONE', ( #33410, #1045, #46426, #4156 ) ) ;
#33205=ADVANCED_FACE ( 'NONE', ( #28156 ), #15576, .T. ) ;
#33308=AXIS2_PLACEMENT_3D ( 'NONE', #19748, #31288, #42289 ) ;
#33360=EDGE_LOOP ( 'NONE', ( #18841, #35667, #47204, #12115 ) ) ;
#33397=CARTESIAN_POINT ( 'NONE',  ( 0.000000000000000000, -0.8299999999999999600, -1.199999999999999956 ) ) ;
#33410=ORIENTED_EDGE ( 'NONE', *, *, #13818, .T. ) ;
#33451=FILL_AREA_STYLE_COLOUR ( '', #24229 ) ;
#33523=UNCERTAINTY_MEASURE_WITH_UNIT (LENGTH_MEASURE( 1.000000000000000082E-05 ), #40232, 'distance_accuracy_value', 'NONE');
#33605=ORIENTED_EDGE ( 'NONE', *, *, #12412, .F. ) ;
#33625=LINE ( 'NONE', #10881, #25851 ) ;
#33634=CARTESIAN_POINT ( 'NONE',  ( -1.250000000000000444, -16.78109714094927085, -1.199999999999999956 ) ) ;
#33792=EDGE_LOOP ( 'NONE', ( #10112, #29799 ) ) ;
#33812=DIRECTION ( 'NONE',  ( 1.000000000000000000, 0.000000000000000000, 0.000000000000000000 ) ) ;
#33846=CARTESIAN_POINT ( 'NONE',  ( -4.250000000000000000, -13.95926121303099343, 0.000000000000000000 ) ) ;
#33879=PLANE ( 'NONE',  #10632 ) ;
#33900=CARTESIAN_POINT ( 'NONE',  ( 8.452893869119503023, -12.51233732111638375, -1.199999999999999956 ) ) ;
#33921=PRESENTATION_STYLE_ASSIGNMENT (( #18988 ) ) ;
#33972=VECTOR ( 'NONE', #21228, 1000.000000000000000 ) ;
#34094=DIRECTION ( 'NONE',  ( 0.1736481776669309418, -0.9848077530122080203, 0.000000000000000000 ) ) ;
#34123=DIRECTION ( 'NONE',  ( -1.000000000000000000, 0.000000000000000000, 0.000000000000000000 ) ) ;
#34167=DIRECTION ( 'NONE',  ( 0.000000000000000000, 0.000000000000000000, 1.000000000000000000 ) ) ;
#34172=CIRCLE ( 'NONE', #1343, 11.59999999999999964 ) ;
#34279=FACE_OUTER_BOUND ( 'NONE', #33180, .T. ) ;
#34285=CIRCLE ( 'NONE', #46789, 0.9999999999999991118 ) ;
#34313=ORIENTED_EDGE ( 'NONE', *, *, #46853, .F. ) ;
#34435=ORIENTED_EDGE ( 'NONE', *, *, #19673, .T. ) ;
#34480=DIRECTION ( 'NONE',  ( 0.000000000000000000, 0.000000000000000000, 1.000000000000000000 ) ) ;
#34595=DIRECTION ( 'NONE',  ( 0.000000000000000000, 0.000000000000000000, 1.000000000000000000 ) ) ;
#34690=ORIENTED_EDGE ( 'NONE', *, *, #46853, .T. ) ;
#34696=ORIENTED_EDGE ( 'NONE', *, *, #2932, .T. ) ;
#34732=CARTESIAN_POINT ( 'NONE',  ( 0.000000000000000000, -0.8299999999999999600, 0.000000000000000000 ) ) ;
#34775=CARTESIAN_POINT ( 'NONE',  ( -4.250000000000000000, -13.95926121303099343, -1.199999999999999956 ) ) ;
#34788=LINE ( 'NONE', #12528, #8488 ) ;
#34839=EDGE_CURVE ( 'NONE', #9856, #17154, #43534, .T. ) ;
#34859=ORIENTED_EDGE ( 'NONE', *, *, #41027, .T. ) ;
#34976=CYLINDRICAL_SURFACE ( 'NONE', #29273, 1.000000000000000000 ) ;
#35150=SURFACE_SIDE_STYLE ('',( #31262 ) ) ;
#35233=CIRCLE ( 'NONE', #18040, 1.000000000000000888 ) ;
#35457=DIRECTION ( 'NONE',  ( -0.000000000000000000, -0.000000000000000000, -1.000000000000000000 ) ) ;
#35571=DIRECTION ( 'NONE',  ( 0.000000000000000000, 0.000000000000000000, 1.000000000000000000 ) ) ;
#35667=ORIENTED_EDGE ( 'NONE', *, *, #15197, .F. ) ;
#35857=DIRECTION ( 'NONE',  ( 0.000000000000000000, 0.000000000000000000, 1.000000000000000000 ) ) ;
#35872=CARTESIAN_POINT ( 'NONE',  ( 0.000000000000000000, -0.8299999999999999600, 0.000000000000000000 ) ) ;
#35924=DIRECTION ( 'NONE',  ( 1.000000000000000000, 0.000000000000000000, 0.000000000000000000 ) ) ;
#35955=ORIENTED_EDGE ( 'NONE', *, *, #36120, .T. ) ;
#35958=EDGE_CURVE ( 'NONE', #29152, #17248, #29605, .T. ) ;
#36059=ORIENTED_EDGE ( 'NONE', *, *, #43448, .T. ) ;
#36111=EDGE_LOOP ( 'NONE', ( #28250, #33605, #13921, #25572 ) ) ;
#36120=EDGE_CURVE ( 'NONE', #7668, #17290, #6174, .T. ) ;
#36144=VERTEX_POINT ( 'NONE', #40582 ) ;
#36155=VERTEX_POINT ( 'NONE', #36892 ) ;
#36205=CARTESIAN_POINT ( 'NONE',  ( 0.000000000000000000, 0.000000000000000000, 0.000000000000000000 ) ) ;
#36270=CARTESIAN_POINT ( 'NONE',  ( 6.509281303079589520, -14.89695620656361008, -1.199999999999999956 ) ) ;
#36297=AXIS2_PLACEMENT_3D ( 'NONE', #19267, #19492, #46362 ) ;
#36413=EDGE_CURVE ( 'NONE', #22374, #36155, #12910, .T. ) ;
#36458=DIRECTION ( 'NONE',  ( -1.000000000000000000, -9.814797785686868941E-17, 0.000000000000000000 ) ) ;
#36569=EDGE_CURVE ( 'NONE', #47625, #7708, #11655, .T. ) ;
#36667=ADVANCED_FACE ( 'NONE', ( #41023 ), #22413, .T. ) ;
#36867=FACE_OUTER_BOUND ( 'NONE', #10133, .T. ) ;
#36892=CARTESIAN_POINT ( 'NONE',  ( -3.249999999999999556, -13.95926121303099343, 0.000000000000000000 ) ) ;
#36942=DIRECTION ( 'NONE',  ( 0.000000000000000000, 0.000000000000000000, 1.000000000000000000 ) ) ;
#37040=VECTOR ( 'NONE', #28542, 1000.000000000000000 ) ;
#37200=DIRECTION ( 'NONE',  ( 1.000000000000000000, 0.000000000000000000, 0.000000000000000000 ) ) ;
#37256=DIRECTION ( 'NONE',  ( 1.000000000000000000, 0.000000000000000000, 0.000000000000000000 ) ) ;
#37325=CARTESIAN_POINT ( 'NONE',  ( 3.250000000000000444, -13.95926121303099343, 0.000000000000000000 ) ) ;
#37401=EDGE_CURVE ( 'NONE', #9856, #39253, #28833, .T. ) ;
#37537=CIRCLE ( 'NONE', #25816, 14.09999999999999964 ) ;
#37775=DIRECTION ( 'NONE',  ( 0.000000000000000000, 0.000000000000000000, 1.000000000000000000 ) ) ;
#37826=DIRECTION ( 'NONE',  ( -1.000000000000000000, 3.469446951953614189E-15, 0.000000000000000000 ) ) ;
#37859=LINE ( 'NONE', #12642, #5750 ) ;
#37898=FACE_OUTER_BOUND ( 'NONE', #31770, .T. ) ;
#37900=EDGE_LOOP ( 'NONE', ( #43503, #29344, #34690, #19326 ) ) ;
#37972=CYLINDRICAL_SURFACE ( 'NONE', #46507, 11.59999999999999964 ) ;
#38008=ORIENTED_EDGE ( 'NONE', *, *, #46384, .F. ) ;
#38046=EDGE_CURVE ( 'NONE', #5367, #36144, #38807, .T. ) ;
#38130=ORIENTED_EDGE ( 'NONE', *, *, #35958, .F. ) ;
#38151=DIRECTION ( 'NONE',  ( 0.000000000000000000, 0.000000000000000000, 1.000000000000000000 ) ) ;
#38200=DIRECTION ( 'NONE',  ( 0.000000000000000000, 0.000000000000000000, 1.000000000000000000 ) ) ;
#38313=CARTESIAN_POINT ( 'NONE',  ( 1.250000000000000444, -16.78109714094927085, 0.000000000000000000 ) ) ;
#38450=AXIS2_PLACEMENT_3D ( 'NONE', #46813, #24529, #43383 ) ;
#38653=AXIS2_PLACEMENT_3D ( 'NONE', #10766, #14683, #29598 ) ;
#38805=AXIS2_PLACEMENT_3D ( 'NONE', #16864, #43289, #20517 ) ;
#38807=LINE ( 'NONE', #30983, #40636 ) ;
#38859=ADVANCED_FACE ( 'NONE', ( #680 ), #45235, .F. ) ;
#38927=EDGE_LOOP ( 'NONE', ( #41892, #36059, #47452, #18012 ) ) ;
#38943=ORIENTED_EDGE ( 'NONE', *, *, #6865, .T. ) ;
#38958=LINE ( 'NONE', #42867, #48280 ) ;
#38984=CARTESIAN_POINT ( 'NONE',  ( -14.09999999999999964, 1.726751986797767995E-15, 0.000000000000000000 ) ) ;
#38988=PLANE ( 'NONE',  #38450 ) ;
#38994=CYLINDRICAL_SURFACE ( 'NONE', #13129, 0.5000000000000004441 ) ;
#39003=CARTESIAN_POINT ( 'NONE',  ( 0.000000000000000000, -0.8299999999999999600, -1.199999999999999956 ) ) ;
#39020=AXIS2_PLACEMENT_3D ( 'NONE', #21437, #17272, #47146 ) ;
#39039=CARTESIAN_POINT ( 'NONE',  ( -8.452893869119503023, -12.51233732111638375, -1.199999999999999956 ) ) ;
#39131=CYLINDRICAL_SURFACE ( 'NONE', #38805, 1.000000000000000000 ) ;
#39164=DIRECTION ( 'NONE',  ( 1.000000000000000000, 0.000000000000000000, 0.000000000000000000 ) ) ;
#39233=EDGE_CURVE ( 'NONE', #19393, #25961, #23378, .T. ) ;
#39253=VERTEX_POINT ( 'NONE', #11646 ) ;
#39341=FACE_OUTER_BOUND ( 'NONE', #28805, .T. ) ;
#39342=ORIENTED_EDGE ( 'NONE', *, *, #28471, .F. ) ;
#39404=AXIS2_PLACEMENT_3D ( 'NONE', #289, #23527, #15476 ) ;
#39428=CARTESIAN_POINT ( 'NONE',  ( -11.59999999999999964, -0.8299999999999986278, 0.000000000000000000 ) ) ;
#39528=AXIS2_PLACEMENT_3D ( 'NONE', #45879, #25509, #32153 ) ;
#39550=LINE ( 'NONE', #14560, #19151 ) ;
#39620=ORIENTED_EDGE ( 'NONE', *, *, #36413, .T. ) ;
#39701=ORIENTED_EDGE ( 'NONE', *, *, #8610, .T. ) ;
#39748=MECHANICAL_DESIGN_GEOMETRIC_PRESENTATION_REPRESENTATION('',(#2997),#46795);
#39778=ORIENTED_EDGE ( 'NONE', *, *, #46384, .T. ) ;
#39813=EDGE_LOOP ( 'NONE', ( #22956, #1161, #6777, #25436 ) ) ;
#39841=CARTESIAN_POINT ( 'NONE',  ( 7.468086116107294004, -12.33868914344945189, -1.199999999999999956 ) ) ;
#40228=ORIENTED_EDGE ( 'NONE', *, *, #48290, .T. ) ;
#40232=( LENGTH_UNIT ( ) NAMED_UNIT ( * ) SI_UNIT ( .MILLI., .METRE. ) );
#40292=CARTESIAN_POINT ( 'NONE',  ( 0.000000000000000000, -0.8299999999999999600, -1.199999999999999956 ) ) ;
#40302=ORIENTED_EDGE ( 'NONE', *, *, #47145, .F. ) ;
#40306=AXIS2_PLACEMENT_3D ( 'NONE', #5972, #1802, #46837 ) ;
#40409=UNCERTAINTY_MEASURE_WITH_UNIT (LENGTH_MEASURE( 1.000000000000000082E-05 ), #16559, 'distance_accuracy_value', 'NONE');
#40476=LINE ( 'NONE', #48041, #40869 ) ;
#40495=CARTESIAN_POINT ( 'NONE',  ( -7.893099573151324044, -11.68370571044642503, 0.000000000000000000 ) ) ;
#40504=DIRECTION ( 'NONE',  ( -0.000000000000000000, -0.000000000000000000, -1.000000000000000000 ) ) ;
#40582=CARTESIAN_POINT ( 'NONE',  ( 7.893099573151324044, -11.68370571044642503, -1.199999999999999956 ) ) ;
#40598=DIRECTION ( 'NONE',  ( -1.000000000000000000, 3.469446951953611033E-15, 0.000000000000000000 ) ) ;
#40603=AXIS2_PLACEMENT_3D ( 'NONE', #34775, #41411, #26241 ) ;
#40636=VECTOR ( 'NONE', #1351, 1000.000000000000000 ) ;
#40741=DIRECTION ( 'NONE',  ( 1.000000000000000000, 0.000000000000000000, 0.000000000000000000 ) ) ;
#40869=VECTOR ( 'NONE', #14526, 1000.000000000000114 ) ;
#41023=FACE_OUTER_BOUND ( 'NONE', #12072, .T. ) ;
#41027=EDGE_CURVE ( 'NONE', #15680, #36155, #12596, .T. ) ;
#41030=APPLICATION_CONTEXT ( 'automotive_design' ) ;
#41055=SURFACE_SIDE_STYLE ('',( #48377 ) ) ;
#41087=ORIENTED_EDGE ( 'NONE', *, *, #42049, .F. ) ;
#41112=ORIENTED_EDGE ( 'NONE', *, *, #29464, .T. ) ;
#41242=CARTESIAN_POINT ( 'NONE',  ( 1.250000000000000000, -12.36245420541525597, 0.000000000000000000 ) ) ;
#41261=DIRECTION ( 'NONE',  ( 0.000000000000000000, 0.000000000000000000, 1.000000000000000000 ) ) ;
#41263=DIRECTION ( 'NONE',  ( 0.000000000000000000, 0.000000000000000000, 1.000000000000000000 ) ) ;
#41329=CARTESIAN_POINT ( 'NONE',  ( 0.000000000000000000, -0.8299999999999999600, -1.199999999999999956 ) ) ;
#41357=LINE ( 'NONE', #8045, #42401 ) ;
#41411=DIRECTION ( 'NONE',  ( 0.000000000000000000, 0.000000000000000000, 1.000000000000000000 ) ) ;
#41412=CARTESIAN_POINT ( 'NONE',  ( 4.250000000000000000, -13.95926121303099343, -1.199999999999999956 ) ) ;
#41571=PLANE ( 'NONE',  #33308 ) ;
#41636=VERTEX_POINT ( 'NONE', #47870 ) ;
#41675=ADVANCED_FACE ( 'NONE', ( #24284 ), #38988, .T. ) ;
#41723=EDGE_LOOP ( 'NONE', ( #11165, #30927, #39701, #40302 ) ) ;
#41828=CARTESIAN_POINT ( 'NONE',  ( -4.250000000000000000, -13.95926121303099343, -1.199999999999999956 ) ) ;
#41892=ORIENTED_EDGE ( 'NONE', *, *, #3920, .F. ) ;
#41908=CLOSED_SHELL ( 'NONE', ( #31520, #27107, #25519, #36667, #32962, #47561, #47380, #33205, #38859, #41675, #42740, #24622, #43935, #24753, #16749, #3919, #2586, #46496, #6075, #25643, #6813, #1823 ) ) ;
#42049=EDGE_CURVE ( 'NONE', #39253, #41636, #30380, .T. ) ;
#42161=DIRECTION ( 'NONE',  ( 9.814797785686868941E-17, 1.000000000000000000, -0.000000000000000000 ) ) ;
#42208=EDGE_CURVE ( 'NONE', #17290, #10381, #10354, .T. ) ;
#42246=ORIENTED_EDGE ( 'NONE', *, *, #7946, .T. ) ;
#42280=EDGE_LOOP ( 'NONE', ( #39342, #25428, #16453, #3707 ) ) ;
#42289=DIRECTION ( 'NONE',  ( 0.1736481776669309696, -0.9848077530122080203, 0.000000000000000000 ) ) ;
#42317=DIRECTION ( 'NONE',  ( 1.000000000000000000, 0.000000000000000000, 0.000000000000000000 ) ) ;
#42364=DIRECTION ( 'NONE',  ( 0.000000000000000000, 0.000000000000000000, 1.000000000000000000 ) ) ;
#42396=AXIS2_PLACEMENT_3D ( 'NONE', #14423, #2426, #40598 ) ;
#42401=VECTOR ( 'NONE', #30341, 1000.000000000000000 ) ;
#42461=AXIS2_PLACEMENT_3D ( 'NONE', #15095, #34167, #15348 ) ;
#42512=EDGE_LOOP ( 'NONE', ( #14187, #27122 ) ) ;
#42575=CIRCLE ( 'NONE', #17532, 16.00000000000000000 ) ;
#42602=DIRECTION ( 'NONE',  ( 0.000000000000000000, 0.000000000000000000, 1.000000000000000000 ) ) ;
#42740=ADVANCED_FACE ( 'NONE', ( #36867 ), #19242, .T. ) ;
#42867=CARTESIAN_POINT ( 'NONE',  ( 7.543218489614351263, -11.91259227951415056, -1.199999999999999956 ) ) ;
#43074=VERTEX_POINT ( 'NONE', #14066 ) ;
#43078=CARTESIAN_POINT ( 'NONE',  ( 3.250000000000000444, -13.95926121303099343, -1.199999999999999956 ) ) ;
#43240=VECTOR ( 'NONE', #14139, 1000.000000000000000 ) ;
#43289=DIRECTION ( 'NONE',  ( 0.000000000000000000, 0.000000000000000000, 1.000000000000000000 ) ) ;
#43383=DIRECTION ( 'NONE',  ( 9.814797785686868941E-17, 1.000000000000000000, 0.000000000000000000 ) ) ;
#43448=EDGE_CURVE ( 'NONE', #1286, #6051, #28452, .T. ) ;
#43503=ORIENTED_EDGE ( 'NONE', *, *, #6311, .F. ) ;
#43534=CIRCLE ( 'NONE', #4475, 16.00000000000000000 ) ;
#43570=ORIENTED_EDGE ( 'NONE', *, *, #22195, .F. ) ;
#43694=AXIS2_PLACEMENT_3D ( 'NONE', #34732, #16155, #13913 ) ;
#43738=PLANE ( 'NONE',  #9875 ) ;
#43870=CARTESIAN_POINT ( 'NONE',  ( 14.09999999999999964, 0.000000000000000000, -1.199999999999999956 ) ) ;
#43935=ADVANCED_FACE ( 'NONE', ( #30477 ), #7950, .T. ) ;
#43962=ORIENTED_EDGE ( 'NONE', *, *, #44215, .T. ) ;
#44016=CARTESIAN_POINT ( 'NONE',  ( -6.509281303079589520, -14.89695620656361008, -1.199999999999999956 ) ) ;
#44088=EDGE_CURVE ( 'NONE', #18357, #25916, #39550, .T. ) ;
#44093=DIRECTION ( 'NONE',  ( 0.000000000000000000, 0.000000000000000000, 1.000000000000000000 ) ) ;
#44178=CARTESIAN_POINT ( 'NONE',  ( -4.250000000000000000, -13.95926121303099343, -1.199999999999999956 ) ) ;
#44215=EDGE_CURVE ( 'NONE', #28409, #29152, #33149, .T. ) ;
#44265=ORIENTED_EDGE ( 'NONE', *, *, #43448, .F. ) ;
#44293=CYLINDRICAL_SURFACE ( 'NONE', #38653, 0.5000000000000004441 ) ;
#44357=EDGE_CURVE ( 'NONE', #4532, #12258, #18920, .T. ) ;
#44396=LINE ( 'NONE', #19166, #32413 ) ;
#44448=ORIENTED_EDGE ( 'NONE', *, *, #42208, .T. ) ;
#44558=ORIENTED_EDGE ( 'NONE', *, *, #42049, .T. ) ;
#44738=ORIENTED_EDGE ( 'NONE', *, *, #44357, .F. ) ;
#44795=ORIENTED_EDGE ( 'NONE', *, *, #12124, .F. ) ;
#45141=DIRECTION ( 'NONE',  ( 0.000000000000000000, 0.000000000000000000, 1.000000000000000000 ) ) ;
#45154=FACE_OUTER_BOUND ( 'NONE', #17717, .T. ) ;
#45235=CYLINDRICAL_SURFACE ( 'NONE', #24292, 11.59999999999999964 ) ;
#45268=VECTOR ( 'NONE', #13141, 1000.000000000000000 ) ;
#45354=VERTEX_POINT ( 'NONE', #7206 ) ;
#45397=DIRECTION ( 'NONE',  ( 1.000000000000000000, 0.000000000000000000, 0.000000000000000000 ) ) ;
#45426=CARTESIAN_POINT ( 'NONE',  ( 1.250000000000000000, -12.36245420541525597, -1.199999999999999956 ) ) ;
#45435=AXIS2_PLACEMENT_3D ( 'NONE', #36205, #24722, #39164 ) ;
#45438=DIRECTION ( 'NONE',  ( -1.000000000000000000, 0.000000000000000000, 0.000000000000000000 ) ) ;
#45515=ORIENTED_EDGE ( 'NONE', *, *, #22195, .T. ) ;
#45573=AXIS2_PLACEMENT_3D ( 'NONE', #33397, #40504, #10393 ) ;
#45645=EDGE_CURVE ( 'NONE', #6291, #441, #31724, .T. ) ;
#45694=CARTESIAN_POINT ( 'NONE',  ( 1.250000000000000000, -12.36245420541525597, -1.199999999999999956 ) ) ;
#45879=CARTESIAN_POINT ( 'NONE',  ( -4.250000000000000000, -13.95926121303099343, -1.199999999999999956 ) ) ;
#45926=( NAMED_UNIT ( * ) SI_UNIT ( $, .STERADIAN. ) SOLID_ANGLE_UNIT ( ) );
#46009=FACE_OUTER_BOUND ( 'NONE', #42280, .T. ) ;
#46362=DIRECTION ( 'NONE',  ( -1.000000000000000000, 0.000000000000000000, 0.000000000000000000 ) ) ;
#46384=EDGE_CURVE ( 'NONE', #12258, #39253, #15175, .T. ) ;
#46426=ORIENTED_EDGE ( 'NONE', *, *, #12444, .F. ) ;
#46451=DIRECTION ( 'NONE',  ( 0.1736481776669309696, 0.9848077530122080203, 0.000000000000000000 ) ) ;
#46496=ADVANCED_FACE ( 'NONE', ( #12703 ), #39131, .F. ) ;
#46507=AXIS2_PLACEMENT_3D ( 'NONE', #23756, #42364, #27202 ) ;
#46789=AXIS2_PLACEMENT_3D ( 'NONE', #39039, #23868, #5506 ) ;
#46795=( GEOMETRIC_REPRESENTATION_CONTEXT ( 3 ) GLOBAL_UNCERTAINTY_ASSIGNED_CONTEXT ( ( #40409 ) ) GLOBAL_UNIT_ASSIGNED_CONTEXT ( ( #16559, #1143, #16094 ) ) REPRESENTATION_CONTEXT ( 'NONE', 'WORKASPACE' ) );
#46813=CARTESIAN_POINT ( 'NONE',  ( -1.250000000000000000, -12.36245420541525597, -1.199999999999999956 ) ) ;
#46837=DIRECTION ( 'NONE',  ( 1.000000000000000000, 0.000000000000000000, 0.000000000000000000 ) ) ;
#46853=EDGE_CURVE ( 'NONE', #31655, #45354, #658, .T. ) ;
#46862=FACE_BOUND ( 'NONE', #2772, .T. ) ;
#46951=LINE ( 'NONE', #28594, #33972 ) ;
#46988=DIRECTION ( 'NONE',  ( -1.000000000000000000, 0.000000000000000000, 0.000000000000000000 ) ) ;
#47029=ORIENTED_EDGE ( 'NONE', *, *, #7421, .T. ) ;
#47145=EDGE_CURVE ( 'NONE', #43074, #11482, #34172, .T. ) ;
#47146=DIRECTION ( 'NONE',  ( -1.000000000000000000, 0.000000000000000000, 0.000000000000000000 ) ) ;
#47204=ORIENTED_EDGE ( 'NONE', *, *, #21900, .T. ) ;
#47247=VERTEX_POINT ( 'NONE', #37325 ) ;
#47310=DIRECTION ( 'NONE',  ( -0.000000000000000000, -0.000000000000000000, -1.000000000000000000 ) ) ;
#47380=ADVANCED_FACE ( 'NONE', ( #19663 ), #17148, .T. ) ;
#47452=ORIENTED_EDGE ( 'NONE', *, *, #22555, .T. ) ;
#47456=DIRECTION ( 'NONE',  ( 0.000000000000000000, 0.000000000000000000, 1.000000000000000000 ) ) ;
#47561=ADVANCED_FACE ( 'NONE', ( #25683 ), #10778, .F. ) ;
#47625=VERTEX_POINT ( 'NONE', #8535 ) ;
#47696=CYLINDRICAL_SURFACE ( 'NONE', #15061, 1.000000000000000000 ) ;
#47721=AXIS2_PLACEMENT_3D ( 'NONE', #17591, #47456, #2902 ) ;
#47742=ORIENTED_EDGE ( 'NONE', *, *, #21564, .T. ) ;
#47870=CARTESIAN_POINT ( 'NONE',  ( -7.001685179585692254, -14.98378029539707512, 0.000000000000000000 ) ) ;
#48041=CARTESIAN_POINT ( 'NONE',  ( 7.543218489614351263, -11.91259227951415056, 0.000000000000000000 ) ) ;
#48254=EDGE_LOOP ( 'NONE', ( #24215, #44738, #4843, #22582 ) ) ;
#48280=VECTOR ( 'NONE', #9319, 1000.000000000000114 ) ;
#48283=SHAPE_DEFINITION_REPRESENTATION ( #28461, #21223 ) ;
#48290=EDGE_CURVE ( 'NONE', #17154, #18357, #34788, .T. ) ;
#48377=SURFACE_STYLE_FILL_AREA ( #403 ) ;
ENDSEC;
END-ISO-10303-21;
